ISO-10303-21;
HEADER;
/* Generated by software containing ST-Developer
 * from STEP Tools, Inc. (www.steptools.com) 
 */

FILE_DESCRIPTION(
/* description */ ('PAT-091'),
/* implementation_level */ '2;1');

FILE_NAME(
/* name */ 'Plain pivot bush (4).step',
/* time_stamp */ '2026-10-27T15:34:44-07:00',
/* author */ (''),
/* organization */ (''),
/* preprocessor_version */ 'ST-DEVELOPER v20.2',
/* originating_system */ 'Autodesk Translation Framework v15.17.0.0',
/* authorisation */ '');

FILE_SCHEMA (('AUTOMOTIVE_DESIGN { 1 0 10303 214 3 1 1 }'));
ENDSEC;

DATA;
#10=MECHANICAL_DESIGN_GEOMETRIC_PRESENTATION_REPRESENTATION('',(#1033),#25100);
#813=SHAPE_REPRESENTATION_RELATIONSHIP('SRR','None',#25579,#923);
#923=ADVANCED_BREP_SHAPE_REPRESENTATION('',(#1155),#25049);
#1033=STYLED_ITEM('',(#26177),#1155);
#1155=MANIFOLD_SOLID_BREP('Body1',#13312);
#1504=FACE_BOUND('',#3663,.T.);
#1505=FACE_BOUND('',#3665,.T.);
#1915=PLANE('',#15585);
#1916=PLANE('',#15586);
#2553=FACE_OUTER_BOUND('',#3660,.T.);
#2554=FACE_OUTER_BOUND('',#3661,.T.);
#2555=FACE_OUTER_BOUND('',#3662,.T.);
#2556=FACE_OUTER_BOUND('',#3664,.T.);
#3660=EDGE_LOOP('',(#10954,#10955,#10956,#10957));
#3661=EDGE_LOOP('',(#10958,#10959,#10960,#10961));
#3662=EDGE_LOOP('',(#10962));
#3663=EDGE_LOOP('',(#10963));
#3664=EDGE_LOOP('',(#10964));
#3665=EDGE_LOOP('',(#10965));
#4679=LINE('',#23241,#5419);
#4680=LINE('',#23247,#5420);
#5419=VECTOR('',#19015,0.604999999999997);
#5420=VECTOR('',#19022,1.);
#6036=CIRCLE('',#15580,0.604999999999997);
#6037=CIRCLE('',#15581,0.604999999999997);
#6038=CIRCLE('',#15583,1.);
#6039=CIRCLE('',#15584,1.);
#7041=VERTEX_POINT('',#23238);
#7042=VERTEX_POINT('',#23240);
#7043=VERTEX_POINT('',#23244);
#7044=VERTEX_POINT('',#23246);
#8412=EDGE_CURVE('',#7041,#7041,#6036,.T.);
#8413=EDGE_CURVE('',#7041,#7042,#4679,.T.);
#8414=EDGE_CURVE('',#7042,#7042,#6037,.T.);
#8415=EDGE_CURVE('',#7043,#7043,#6038,.T.);
#8416=EDGE_CURVE('',#7043,#7044,#4680,.T.);
#8417=EDGE_CURVE('',#7044,#7044,#6039,.T.);
#10954=ORIENTED_EDGE('',*,*,#8412,.F.);
#10955=ORIENTED_EDGE('',*,*,#8413,.T.);
#10956=ORIENTED_EDGE('',*,*,#8414,.T.);
#10957=ORIENTED_EDGE('',*,*,#8413,.F.);
#10958=ORIENTED_EDGE('',*,*,#8415,.F.);
#10959=ORIENTED_EDGE('',*,*,#8416,.T.);
#10960=ORIENTED_EDGE('',*,*,#8417,.T.);
#10961=ORIENTED_EDGE('',*,*,#8416,.F.);
#10962=ORIENTED_EDGE('',*,*,#8415,.T.);
#10963=ORIENTED_EDGE('',*,*,#8412,.T.);
#10964=ORIENTED_EDGE('',*,*,#8417,.F.);
#10965=ORIENTED_EDGE('',*,*,#8414,.F.);
#12281=CYLINDRICAL_SURFACE('',#15579,0.604999999999997);
#12282=CYLINDRICAL_SURFACE('',#15582,1.);
#12920=ADVANCED_FACE('',(#2553),#12281,.F.);
#12921=ADVANCED_FACE('',(#2554),#12282,.T.);
#12922=ADVANCED_FACE('',(#2555,#1504),#1915,.T.);
#12923=ADVANCED_FACE('',(#2556,#1505),#1916,.F.);
#13312=CLOSED_SHELL('',(#12920,#12921,#12922,#12923));
#15578=AXIS2_PLACEMENT_3D('',#23236,#19009,#19010);
#15579=AXIS2_PLACEMENT_3D('',#23237,#19011,#19012);
#15580=AXIS2_PLACEMENT_3D('',#23239,#19013,#19014);
#15581=AXIS2_PLACEMENT_3D('',#23242,#19016,#19017);
#15582=AXIS2_PLACEMENT_3D('',#23243,#19018,#19019);
#15583=AXIS2_PLACEMENT_3D('',#23245,#19020,#19021);
#15584=AXIS2_PLACEMENT_3D('',#23248,#19023,#19024);
#15585=AXIS2_PLACEMENT_3D('',#23249,#19025,#19026);
#15586=AXIS2_PLACEMENT_3D('',#23250,#19027,#19028);
#19009=DIRECTION('axis',(0.,0.,1.));
#19010=DIRECTION('refdir',(1.,0.,0.));
#19011=DIRECTION('center_axis',(0.,1.,0.));
#19012=DIRECTION('ref_axis',(1.,0.,0.));
#19013=DIRECTION('center_axis',(0.,-1.,0.));
#19014=DIRECTION('ref_axis',(1.,0.,0.));
#19015=DIRECTION('',(0.,-1.,0.));
#19016=DIRECTION('center_axis',(0.,-1.,0.));
#19017=DIRECTION('ref_axis',(1.,0.,0.));
#19018=DIRECTION('center_axis',(0.,1.,0.));
#19019=DIRECTION('ref_axis',(1.,0.,0.));
#19020=DIRECTION('center_axis',(0.,1.,0.));
#19021=DIRECTION('ref_axis',(1.,0.,0.));
#19022=DIRECTION('',(0.,-1.,0.));
#19023=DIRECTION('center_axis',(0.,1.,0.));
#19024=DIRECTION('ref_axis',(1.,0.,0.));
#19025=DIRECTION('center_axis',(0.,1.,0.));
#19026=DIRECTION('ref_axis',(1.,0.,0.));
#19027=DIRECTION('center_axis',(0.,1.,0.));
#19028=DIRECTION('ref_axis',(1.,0.,0.));
#23236=CARTESIAN_POINT('',(0.,0.,0.));
#23237=CARTESIAN_POINT('Origin',(38.7298334620742,5.,13.));
#23238=CARTESIAN_POINT('',(38.1248334620742,6.,13.));
#23239=CARTESIAN_POINT('Origin',(38.7298334620742,6.,13.));
#23240=CARTESIAN_POINT('',(38.1248334620742,5.,13.));
#23241=CARTESIAN_POINT('',(38.1248334620742,5.,13.));
#23242=CARTESIAN_POINT('Origin',(38.7298334620742,5.,13.));
#23243=CARTESIAN_POINT('Origin',(38.7298334620742,5.,13.));
#23244=CARTESIAN_POINT('',(37.7298334620742,6.,13.));
#23245=CARTESIAN_POINT('Origin',(38.7298334620742,6.,13.));
#23246=CARTESIAN_POINT('',(37.7298334620742,5.,13.));
#23247=CARTESIAN_POINT('',(37.7298334620742,5.,13.));
#23248=CARTESIAN_POINT('Origin',(38.7298334620742,5.,13.));
#23249=CARTESIAN_POINT('Origin',(38.7298334620742,6.,13.));
#23250=CARTESIAN_POINT('Origin',(38.7298334620742,5.,13.));
#24928=UNCERTAINTY_MEASURE_WITH_UNIT(LENGTH_MEASURE(0.001),#25101,
'DISTANCE_ACCURACY_VALUE',
'Maximum model space distance between geometric entities at asserted c
onnectivities');
#24979=UNCERTAINTY_MEASURE_WITH_UNIT(LENGTH_MEASURE(0.001),#25101,
'DISTANCE_ACCURACY_VALUE',
'Maximum model space distance between geometric entities at asserted c
onnectivities');
#25049=(
GEOMETRIC_REPRESENTATION_CONTEXT(3)
GLOBAL_UNCERTAINTY_ASSIGNED_CONTEXT((#24928))
GLOBAL_UNIT_ASSIGNED_CONTEXT((#25101,#25103,#25104))
REPRESENTATION_CONTEXT('','3D')
);
#25100=(
GEOMETRIC_REPRESENTATION_CONTEXT(3)
GLOBAL_UNCERTAINTY_ASSIGNED_CONTEXT((#24979))
GLOBAL_UNIT_ASSIGNED_CONTEXT((#25101,#25103,#25104))
REPRESENTATION_CONTEXT('','3D')
);
#25101=(
LENGTH_UNIT()
NAMED_UNIT(*)
SI_UNIT(.CENTI.,.METRE.)
);
#25103=(
NAMED_UNIT(*)
PLANE_ANGLE_UNIT()
SI_UNIT($,.RADIAN.)
);
#25104=(
NAMED_UNIT(*)
SI_UNIT($,.STERADIAN.)
SOLID_ANGLE_UNIT()
);
#25174=SHAPE_DEFINITION_REPRESENTATION(#25296,#25579);
#25296=PRODUCT_DEFINITION_SHAPE('',$,#25700);
#25579=SHAPE_REPRESENTATION('',(#15578),#25049);
#25630=PRODUCT_DEFINITION_CONTEXT('part definition',#25992,'design');
#25700=PRODUCT_DEFINITION('Plain pivot bush (4)','Plain pivot bush (4)',#25820,
#25630);
#25820=PRODUCT_DEFINITION_FORMATION('',$,#26063);
#25992=APPLICATION_CONTEXT(
'Core Data for Automotive Mechanical Design Process');
#25993=PRODUCT_CONTEXT('part definition',#25992,'mechanical');
#26063=PRODUCT('Plain pivot bush (4)','Plain pivot bush (4)',
'Plain pivot bush (4)',(#25993));
#26171=COLOUR_RGB('Light Blue',0.38,0.62,0.78);
#26172=FILL_AREA_STYLE_COLOUR('',#26171);
#26173=FILL_AREA_STYLE('',(#26172));
#26174=SURFACE_STYLE_FILL_AREA(#26173);
#26175=SURFACE_SIDE_STYLE('',(#26174));
#26176=SURFACE_STYLE_USAGE(.BOTH.,#26175);
#26177=PRESENTATION_STYLE_ASSIGNMENT((#26176));
ENDSEC;
END-ISO-10303-21;
